ISO-10303-21;
HEADER;
/* Generated by software containing ST-Developer
 * from STEP Tools, Inc. (www.steptools.com) 
 */

FILE_DESCRIPTION(
/* description */ (''),
/* implementation_level */ '2;1');

FILE_NAME(
/* name */ 'Pin_02.step',
/* time_stamp */ '2026-10-04T12:17:52-07:00',
/* author */ (''),
/* organization */ (''),
/* preprocessor_version */ 'ST-DEVELOPER v20.2',
/* originating_system */ 'Autodesk Translation Framework v15.15.0.0',
/* authorisation */ '');

FILE_SCHEMA (('AUTOMOTIVE_DESIGN { 1 0 10303 214 3 1 1 }'));
ENDSEC;

DATA;
#10=MECHANICAL_DESIGN_GEOMETRIC_PRESENTATION_REPRESENTATION('',(#67),#1602);
#51=SHAPE_REPRESENTATION_RELATIONSHIP('SRR','None',#1638,#59);
#59=ADVANCED_BREP_SHAPE_REPRESENTATION('',(#75),#1598);
#67=STYLED_ITEM('',(#1684),#75);
#75=MANIFOLD_SOLID_BREP('Body1',#778);
#119=CIRCLE('',#936,2.5);
#120=CIRCLE('',#938,2.5);
#148=CYLINDRICAL_SURFACE('',#937,2.5);
#187=FACE_OUTER_BOUND('',#242,.T.);
#188=FACE_OUTER_BOUND('',#243,.T.);
#189=FACE_OUTER_BOUND('',#244,.T.);
#242=EDGE_LOOP('',(#660));
#243=EDGE_LOOP('',(#661,#662,#663,#664));
#244=EDGE_LOOP('',(#665));
#305=LINE('',#1528,#354);
#354=VECTOR('',#1153,2.5);
#409=VERTEX_POINT('',#1523);
#410=VERTEX_POINT('',#1526);
#495=EDGE_CURVE('',#409,#409,#119,.T.);
#496=EDGE_CURVE('',#410,#410,#120,.T.);
#497=EDGE_CURVE('',#410,#409,#305,.T.);
#660=ORIENTED_EDGE('',*,*,#495,.T.);
#661=ORIENTED_EDGE('',*,*,#496,.F.);
#662=ORIENTED_EDGE('',*,*,#497,.T.);
#663=ORIENTED_EDGE('',*,*,#495,.F.);
#664=ORIENTED_EDGE('',*,*,#497,.F.);
#665=ORIENTED_EDGE('',*,*,#496,.T.);
#719=PLANE('',#935);
#720=PLANE('',#939);
#759=ADVANCED_FACE('',(#187),#719,.F.);
#760=ADVANCED_FACE('',(#188),#148,.T.);
#761=ADVANCED_FACE('',(#189),#720,.T.);
#778=CLOSED_SHELL('',(#759,#760,#761));
#934=AXIS2_PLACEMENT_3D('',#1521,#1143,#1144);
#935=AXIS2_PLACEMENT_3D('',#1522,#1145,#1146);
#936=AXIS2_PLACEMENT_3D('',#1524,#1147,#1148);
#937=AXIS2_PLACEMENT_3D('',#1525,#1149,#1150);
#938=AXIS2_PLACEMENT_3D('',#1527,#1151,#1152);
#939=AXIS2_PLACEMENT_3D('',#1529,#1154,#1155);
#1143=DIRECTION('axis',(0.,0.,1.));
#1144=DIRECTION('refdir',(1.,0.,0.));
#1145=DIRECTION('center_axis',(0.,0.,1.));
#1146=DIRECTION('ref_axis',(1.,0.,0.));
#1147=DIRECTION('center_axis',(0.,0.,-1.));
#1148=DIRECTION('ref_axis',(1.,0.,0.));
#1149=DIRECTION('center_axis',(0.,0.,1.));
#1150=DIRECTION('ref_axis',(1.,0.,0.));
#1151=DIRECTION('center_axis',(0.,0.,1.));
#1152=DIRECTION('ref_axis',(1.,0.,0.));
#1153=DIRECTION('',(0.,0.,-1.));
#1154=DIRECTION('center_axis',(0.,0.,1.));
#1155=DIRECTION('ref_axis',(1.,0.,0.));
#1521=CARTESIAN_POINT('',(0.,0.,0.));
#1522=CARTESIAN_POINT('Origin',(0.,0.,94.6));
#1523=CARTESIAN_POINT('',(-2.5,-3.06161699786838E-16,94.6));
#1524=CARTESIAN_POINT('Origin',(0.,0.,94.6));
#1525=CARTESIAN_POINT('Origin',(0.,0.,96.6));
#1526=CARTESIAN_POINT('',(-2.5,-3.06161699786838E-16,102.1));
#1527=CARTESIAN_POINT('Origin',(0.,0.,102.1));
#1528=CARTESIAN_POINT('',(-2.5,-3.06161699786838E-16,96.6));
#1529=CARTESIAN_POINT('Origin',(0.,0.,102.1));
#1588=UNCERTAINTY_MEASURE_WITH_UNIT(LENGTH_MEASURE(0.01),#1603,
'DISTANCE_ACCURACY_VALUE',
'Maximum model space distance between geometric entities at asserted c
onnectivities');
#1592=UNCERTAINTY_MEASURE_WITH_UNIT(LENGTH_MEASURE(0.01),#1603,
'DISTANCE_ACCURACY_VALUE',
'Maximum model space distance between geometric entities at asserted c
onnectivities');
#1598=(
GEOMETRIC_REPRESENTATION_CONTEXT(3)
GLOBAL_UNCERTAINTY_ASSIGNED_CONTEXT((#1588))
GLOBAL_UNIT_ASSIGNED_CONTEXT((#1603,#1605,#1606))
REPRESENTATION_CONTEXT('','3D')
);
#1602=(
GEOMETRIC_REPRESENTATION_CONTEXT(3)
GLOBAL_UNCERTAINTY_ASSIGNED_CONTEXT((#1592))
GLOBAL_UNIT_ASSIGNED_CONTEXT((#1603,#1605,#1606))
REPRESENTATION_CONTEXT('','3D')
);
#1603=(
LENGTH_UNIT()
NAMED_UNIT(*)
SI_UNIT(.MILLI.,.METRE.)
);
#1605=(
NAMED_UNIT(*)
PLANE_ANGLE_UNIT()
SI_UNIT($,.RADIAN.)
);
#1606=(
NAMED_UNIT(*)
SI_UNIT($,.STERADIAN.)
SOLID_ANGLE_UNIT()
);
#1612=SHAPE_DEFINITION_REPRESENTATION(#1621,#1638);
#1621=PRODUCT_DEFINITION_SHAPE('',$,#1648);
#1638=SHAPE_REPRESENTATION('',(#934),#1598);
#1642=PRODUCT_DEFINITION_CONTEXT('part definition',#1671,'design');
#1648=PRODUCT_DEFINITION('Pin_02','Pin_02',#1657,#1642);
#1657=PRODUCT_DEFINITION_FORMATION('',$,#1678);
#1671=APPLICATION_CONTEXT(
'Core Data for Automotive Mechanical Design Process');
#1672=PRODUCT_CONTEXT('part definition',#1671,'mechanical');
#1678=PRODUCT('Pin_02','Pin_02',$,(#1672));
#1684=PRESENTATION_STYLE_ASSIGNMENT((#1688));
#1688=SURFACE_STYLE_USAGE(.BOTH.,#1692);
#1692=SURFACE_SIDE_STYLE('',(#1696));
#1696=SURFACE_STYLE_FILL_AREA(#1700);
#1700=FILL_AREA_STYLE('Opaque(160,160,160)',(#1704));
#1704=FILL_AREA_STYLE_COLOUR('Opaque(160,160,160)',#1708);
#1708=COLOUR_RGB('Opaque(160,160,160)', 0.66274510, 0.83137255, 0.94901961);
ENDSEC;
END-ISO-10303-21;
